ISO-10303-21;
HEADER;
/* Generated by software containing ST-Developer
 * from STEP Tools, Inc. (www.steptools.com) 
 */

FILE_DESCRIPTION(
/* description */ ('Door-style hinge test fixture with detent'),
/* implementation_level */ '2;1');

FILE_NAME(
/* name */ 'M4x10 Cap Screw.step',
/* time_stamp */ '2026-10-28T03:24:57-07:00',
/* author */ (''),
/* organization */ (''),
/* preprocessor_version */ 'ST-DEVELOPER v20.2',
/* originating_system */ 'Autodesk Translation Framework v15.17.0.0',
/* authorisation */ '');

FILE_SCHEMA (('AUTOMOTIVE_DESIGN { 1 0 10303 214 3 1 1 }'));
ENDSEC;

DATA;
#10=MECHANICAL_DESIGN_GEOMETRIC_PRESENTATION_REPRESENTATION('',(#355),#9813);
#208=CONICAL_SURFACE('',#5589,0.325,0.785398163397448);
#209=CONICAL_SURFACE('',#5593,0.335,0.785398163397448);
#210=CONICAL_SURFACE('',#5597,0.21,0.463647609000806);
#216=ORIENTED_CLOSED_SHELL('',*,#4787,.F.);
#219=BREP_WITH_VOIDS('Body1',#4788,(#216));
#284=SHAPE_REPRESENTATION_RELATIONSHIP('SRR','None',#9962,#315);
#315=ADVANCED_BREP_SHAPE_REPRESENTATION('',(#219),#9805);
#355=STYLED_ITEM('',(#10190),#219);
#477=FACE_BOUND('',#1253,.T.);
#622=PLANE('',#5577);
#623=PLANE('',#5578);
#624=PLANE('',#5579);
#625=PLANE('',#5580);
#626=PLANE('',#5581);
#627=PLANE('',#5582);
#628=PLANE('',#5583);
#629=PLANE('',#5584);
#630=PLANE('',#5585);
#631=PLANE('',#5587);
#632=PLANE('',#5595);
#876=FACE_OUTER_BOUND('',#1239,.T.);
#877=FACE_OUTER_BOUND('',#1240,.T.);
#878=FACE_OUTER_BOUND('',#1241,.T.);
#879=FACE_OUTER_BOUND('',#1242,.T.);
#880=FACE_OUTER_BOUND('',#1243,.T.);
#881=FACE_OUTER_BOUND('',#1244,.T.);
#882=FACE_OUTER_BOUND('',#1245,.T.);
#883=FACE_OUTER_BOUND('',#1246,.T.);
#884=FACE_OUTER_BOUND('',#1247,.T.);
#885=FACE_OUTER_BOUND('',#1248,.T.);
#886=FACE_OUTER_BOUND('',#1249,.T.);
#887=FACE_OUTER_BOUND('',#1250,.T.);
#888=FACE_OUTER_BOUND('',#1251,.T.);
#889=FACE_OUTER_BOUND('',#1252,.T.);
#890=FACE_OUTER_BOUND('',#1254,.T.);
#891=FACE_OUTER_BOUND('',#1255,.T.);
#1239=EDGE_LOOP('',(#4111,#4112,#4113,#4114));
#1240=EDGE_LOOP('',(#4115,#4116,#4117,#4118));
#1241=EDGE_LOOP('',(#4119,#4120,#4121,#4122));
#1242=EDGE_LOOP('',(#4123,#4124,#4125,#4126));
#1243=EDGE_LOOP('',(#4127,#4128,#4129,#4130));
#1244=EDGE_LOOP('',(#4131,#4132,#4133,#4134));
#1245=EDGE_LOOP('',(#4135,#4136,#4137,#4138,#4139,#4140));
#1246=EDGE_LOOP('',(#4141,#4142,#4143,#4144,#4145,#4146));
#1247=EDGE_LOOP('',(#4147));
#1248=EDGE_LOOP('',(#4148));
#1249=EDGE_LOOP('',(#4149,#4150,#4151,#4152));
#1250=EDGE_LOOP('',(#4153,#4154,#4155,#4156));
#1251=EDGE_LOOP('',(#4157,#4158,#4159,#4160));
#1252=EDGE_LOOP('',(#4161));
#1253=EDGE_LOOP('',(#4162));
#1254=EDGE_LOOP('',(#4163,#4164,#4165,#4166));
#1255=EDGE_LOOP('',(#4167,#4168,#4169,#4170));
#1573=LINE('',#9360,#1893);
#1574=LINE('',#9362,#1894);
#1575=LINE('',#9364,#1895);
#1576=LINE('',#9365,#1896);
#1577=LINE('',#9368,#1897);
#1578=LINE('',#9370,#1898);
#1579=LINE('',#9371,#1899);
#1580=LINE('',#9374,#1900);
#1581=LINE('',#9376,#1901);
#1582=LINE('',#9377,#1902);
#1583=LINE('',#9380,#1903);
#1584=LINE('',#9382,#1904);
#1585=LINE('',#9383,#1905);
#1586=LINE('',#9386,#1906);
#1587=LINE('',#9388,#1907);
#1588=LINE('',#9389,#1908);
#1589=LINE('',#9391,#1909);
#1590=LINE('',#9392,#1910);
#1591=LINE('',#9404,#1911);
#1592=LINE('',#9408,#1912);
#1593=LINE('',#9412,#1913);
#1594=LINE('',#9419,#1914);
#1595=LINE('',#9421,#1915);
#1893=VECTOR('',#6870,1.);
#1894=VECTOR('',#6871,1.);
#1895=VECTOR('',#6872,1.);
#1896=VECTOR('',#6873,1.);
#1897=VECTOR('',#6876,1.);
#1898=VECTOR('',#6877,1.);
#1899=VECTOR('',#6878,1.);
#1900=VECTOR('',#6881,1.);
#1901=VECTOR('',#6882,1.);
#1902=VECTOR('',#6883,1.);
#1903=VECTOR('',#6886,1.);
#1904=VECTOR('',#6887,1.);
#1905=VECTOR('',#6888,1.);
#1906=VECTOR('',#6891,1.);
#1907=VECTOR('',#6892,1.);
#1908=VECTOR('',#6893,1.);
#1909=VECTOR('',#6896,1.);
#1910=VECTOR('',#6897,1.);
#1911=VECTOR('',#6914,0.325);
#1912=VECTOR('',#6919,0.35);
#1913=VECTOR('',#6924,0.335);
#1914=VECTOR('',#6933,0.21);
#1915=VECTOR('',#6936,0.2);
#2168=CIRCLE('',#5586,0.1954);
#2169=CIRCLE('',#5588,0.3);
#2170=CIRCLE('',#5590,0.35);
#2171=CIRCLE('',#5592,0.35);
#2172=CIRCLE('',#5594,0.32);
#2173=CIRCLE('',#5596,0.22);
#2174=CIRCLE('',#5598,0.1954);
#2532=VERTEX_POINT('',#9358);
#2533=VERTEX_POINT('',#9359);
#2534=VERTEX_POINT('',#9361);
#2535=VERTEX_POINT('',#9363);
#2536=VERTEX_POINT('',#9367);
#2537=VERTEX_POINT('',#9369);
#2538=VERTEX_POINT('',#9373);
#2539=VERTEX_POINT('',#9375);
#2540=VERTEX_POINT('',#9379);
#2541=VERTEX_POINT('',#9381);
#2542=VERTEX_POINT('',#9385);
#2543=VERTEX_POINT('',#9387);
#2544=VERTEX_POINT('',#9396);
#2545=VERTEX_POINT('',#9399);
#2546=VERTEX_POINT('',#9402);
#2547=VERTEX_POINT('',#9406);
#2548=VERTEX_POINT('',#9410);
#2549=VERTEX_POINT('',#9414);
#2550=VERTEX_POINT('',#9417);
#3072=EDGE_CURVE('',#2532,#2533,#1573,.T.);
#3073=EDGE_CURVE('',#2533,#2534,#1574,.T.);
#3074=EDGE_CURVE('',#2534,#2535,#1575,.T.);
#3075=EDGE_CURVE('',#2532,#2535,#1576,.T.);
#3076=EDGE_CURVE('',#2533,#2536,#1577,.T.);
#3077=EDGE_CURVE('',#2536,#2537,#1578,.T.);
#3078=EDGE_CURVE('',#2537,#2534,#1579,.T.);
#3079=EDGE_CURVE('',#2536,#2538,#1580,.T.);
#3080=EDGE_CURVE('',#2538,#2539,#1581,.T.);
#3081=EDGE_CURVE('',#2539,#2537,#1582,.T.);
#3082=EDGE_CURVE('',#2538,#2540,#1583,.T.);
#3083=EDGE_CURVE('',#2540,#2541,#1584,.T.);
#3084=EDGE_CURVE('',#2541,#2539,#1585,.T.);
#3085=EDGE_CURVE('',#2540,#2542,#1586,.T.);
#3086=EDGE_CURVE('',#2542,#2543,#1587,.T.);
#3087=EDGE_CURVE('',#2543,#2541,#1588,.T.);
#3088=EDGE_CURVE('',#2542,#2532,#1589,.T.);
#3089=EDGE_CURVE('',#2535,#2543,#1590,.T.);
#3090=EDGE_CURVE('',#2544,#2544,#2168,.T.);
#3091=EDGE_CURVE('',#2545,#2545,#2169,.T.);
#3092=EDGE_CURVE('',#2546,#2546,#2170,.T.);
#3093=EDGE_CURVE('',#2546,#2545,#1591,.T.);
#3094=EDGE_CURVE('',#2547,#2547,#2171,.T.);
#3095=EDGE_CURVE('',#2547,#2546,#1592,.T.);
#3096=EDGE_CURVE('',#2548,#2548,#2172,.T.);
#3097=EDGE_CURVE('',#2548,#2547,#1593,.T.);
#3098=EDGE_CURVE('',#2549,#2549,#2173,.T.);
#3099=EDGE_CURVE('',#2550,#2550,#2174,.F.);
#3100=EDGE_CURVE('',#2550,#2549,#1594,.T.);
#3101=EDGE_CURVE('',#2544,#2550,#1595,.T.);
#4111=ORIENTED_EDGE('',*,*,#3072,.T.);
#4112=ORIENTED_EDGE('',*,*,#3073,.T.);
#4113=ORIENTED_EDGE('',*,*,#3074,.T.);
#4114=ORIENTED_EDGE('',*,*,#3075,.F.);
#4115=ORIENTED_EDGE('',*,*,#3076,.T.);
#4116=ORIENTED_EDGE('',*,*,#3077,.T.);
#4117=ORIENTED_EDGE('',*,*,#3078,.T.);
#4118=ORIENTED_EDGE('',*,*,#3073,.F.);
#4119=ORIENTED_EDGE('',*,*,#3079,.T.);
#4120=ORIENTED_EDGE('',*,*,#3080,.T.);
#4121=ORIENTED_EDGE('',*,*,#3081,.T.);
#4122=ORIENTED_EDGE('',*,*,#3077,.F.);
#4123=ORIENTED_EDGE('',*,*,#3082,.T.);
#4124=ORIENTED_EDGE('',*,*,#3083,.T.);
#4125=ORIENTED_EDGE('',*,*,#3084,.T.);
#4126=ORIENTED_EDGE('',*,*,#3080,.F.);
#4127=ORIENTED_EDGE('',*,*,#3085,.T.);
#4128=ORIENTED_EDGE('',*,*,#3086,.T.);
#4129=ORIENTED_EDGE('',*,*,#3087,.T.);
#4130=ORIENTED_EDGE('',*,*,#3083,.F.);
#4131=ORIENTED_EDGE('',*,*,#3088,.T.);
#4132=ORIENTED_EDGE('',*,*,#3075,.T.);
#4133=ORIENTED_EDGE('',*,*,#3089,.T.);
#4134=ORIENTED_EDGE('',*,*,#3086,.F.);
#4135=ORIENTED_EDGE('',*,*,#3088,.F.);
#4136=ORIENTED_EDGE('',*,*,#3085,.F.);
#4137=ORIENTED_EDGE('',*,*,#3082,.F.);
#4138=ORIENTED_EDGE('',*,*,#3079,.F.);
#4139=ORIENTED_EDGE('',*,*,#3076,.F.);
#4140=ORIENTED_EDGE('',*,*,#3072,.F.);
#4141=ORIENTED_EDGE('',*,*,#3089,.F.);
#4142=ORIENTED_EDGE('',*,*,#3074,.F.);
#4143=ORIENTED_EDGE('',*,*,#3078,.F.);
#4144=ORIENTED_EDGE('',*,*,#3081,.F.);
#4145=ORIENTED_EDGE('',*,*,#3084,.F.);
#4146=ORIENTED_EDGE('',*,*,#3087,.F.);
#4147=ORIENTED_EDGE('',*,*,#3090,.F.);
#4148=ORIENTED_EDGE('',*,*,#3091,.F.);
#4149=ORIENTED_EDGE('',*,*,#3092,.F.);
#4150=ORIENTED_EDGE('',*,*,#3093,.T.);
#4151=ORIENTED_EDGE('',*,*,#3091,.T.);
#4152=ORIENTED_EDGE('',*,*,#3093,.F.);
#4153=ORIENTED_EDGE('',*,*,#3094,.F.);
#4154=ORIENTED_EDGE('',*,*,#3095,.T.);
#4155=ORIENTED_EDGE('',*,*,#3092,.T.);
#4156=ORIENTED_EDGE('',*,*,#3095,.F.);
#4157=ORIENTED_EDGE('',*,*,#3096,.F.);
#4158=ORIENTED_EDGE('',*,*,#3097,.T.);
#4159=ORIENTED_EDGE('',*,*,#3094,.T.);
#4160=ORIENTED_EDGE('',*,*,#3097,.F.);
#4161=ORIENTED_EDGE('',*,*,#3096,.T.);
#4162=ORIENTED_EDGE('',*,*,#3098,.F.);
#4163=ORIENTED_EDGE('',*,*,#3099,.F.);
#4164=ORIENTED_EDGE('',*,*,#3100,.T.);
#4165=ORIENTED_EDGE('',*,*,#3098,.T.);
#4166=ORIENTED_EDGE('',*,*,#3100,.F.);
#4167=ORIENTED_EDGE('',*,*,#3090,.T.);
#4168=ORIENTED_EDGE('',*,*,#3101,.T.);
#4169=ORIENTED_EDGE('',*,*,#3099,.T.);
#4170=ORIENTED_EDGE('',*,*,#3101,.F.);
#4445=CYLINDRICAL_SURFACE('',#5591,0.35);
#4446=CYLINDRICAL_SURFACE('',#5599,0.1954);
#4681=ADVANCED_FACE('',(#876),#622,.F.);
#4682=ADVANCED_FACE('',(#877),#623,.F.);
#4683=ADVANCED_FACE('',(#878),#624,.F.);
#4684=ADVANCED_FACE('',(#879),#625,.F.);
#4685=ADVANCED_FACE('',(#880),#626,.F.);
#4686=ADVANCED_FACE('',(#881),#627,.F.);
#4687=ADVANCED_FACE('',(#882),#628,.F.);
#4688=ADVANCED_FACE('',(#883),#629,.F.);
#4689=ADVANCED_FACE('',(#884),#630,.F.);
#4690=ADVANCED_FACE('',(#885),#631,.T.);
#4691=ADVANCED_FACE('',(#886),#208,.T.);
#4692=ADVANCED_FACE('',(#887),#4445,.T.);
#4693=ADVANCED_FACE('',(#888),#209,.T.);
#4694=ADVANCED_FACE('',(#889,#477),#632,.T.);
#4695=ADVANCED_FACE('',(#890),#210,.T.);
#4696=ADVANCED_FACE('',(#891),#4446,.T.);
#4787=CLOSED_SHELL('',(#4681,#4682,#4683,#4684,#4685,#4686,#4687,#4688));
#4788=CLOSED_SHELL('',(#4689,#4690,#4691,#4692,#4693,#4694,#4695,#4696));
#5576=AXIS2_PLACEMENT_3D('',#9356,#6866,#6867);
#5577=AXIS2_PLACEMENT_3D('',#9357,#6868,#6869);
#5578=AXIS2_PLACEMENT_3D('',#9366,#6874,#6875);
#5579=AXIS2_PLACEMENT_3D('',#9372,#6879,#6880);
#5580=AXIS2_PLACEMENT_3D('',#9378,#6884,#6885);
#5581=AXIS2_PLACEMENT_3D('',#9384,#6889,#6890);
#5582=AXIS2_PLACEMENT_3D('',#9390,#6894,#6895);
#5583=AXIS2_PLACEMENT_3D('',#9393,#6898,#6899);
#5584=AXIS2_PLACEMENT_3D('',#9394,#6900,#6901);
#5585=AXIS2_PLACEMENT_3D('',#9395,#6902,#6903);
#5586=AXIS2_PLACEMENT_3D('',#9397,#6904,#6905);
#5587=AXIS2_PLACEMENT_3D('',#9398,#6906,#6907);
#5588=AXIS2_PLACEMENT_3D('',#9400,#6908,#6909);
#5589=AXIS2_PLACEMENT_3D('',#9401,#6910,#6911);
#5590=AXIS2_PLACEMENT_3D('',#9403,#6912,#6913);
#5591=AXIS2_PLACEMENT_3D('',#9405,#6915,#6916);
#5592=AXIS2_PLACEMENT_3D('',#9407,#6917,#6918);
#5593=AXIS2_PLACEMENT_3D('',#9409,#6920,#6921);
#5594=AXIS2_PLACEMENT_3D('',#9411,#6922,#6923);
#5595=AXIS2_PLACEMENT_3D('',#9413,#6925,#6926);
#5596=AXIS2_PLACEMENT_3D('',#9415,#6927,#6928);
#5597=AXIS2_PLACEMENT_3D('',#9416,#6929,#6930);
#5598=AXIS2_PLACEMENT_3D('',#9418,#6931,#6932);
#5599=AXIS2_PLACEMENT_3D('',#9420,#6934,#6935);
#6866=DIRECTION('axis',(0.,0.,1.));
#6867=DIRECTION('refdir',(1.,0.,0.));
#6868=DIRECTION('center_axis',(0.866025403784439,0.,-0.5));
#6869=DIRECTION('ref_axis',(0.5,0.,0.866025403784439));
#6870=DIRECTION('',(-0.5,0.,-0.866025403784439));
#6871=DIRECTION('',(0.,-1.,0.));
#6872=DIRECTION('',(0.5,0.,0.866025403784439));
#6873=DIRECTION('',(0.,-1.,0.));
#6874=DIRECTION('center_axis',(1.60246890531964E-16,0.,-1.));
#6875=DIRECTION('ref_axis',(1.,0.,1.60246890531964E-16));
#6876=DIRECTION('',(-1.,0.,-1.60246890531964E-16));
#6877=DIRECTION('',(0.,-1.,0.));
#6878=DIRECTION('',(1.,0.,1.60246890531964E-16));
#6879=DIRECTION('center_axis',(-0.866025403784439,0.,-0.5));
#6880=DIRECTION('ref_axis',(0.5,0.,-0.866025403784439));
#6881=DIRECTION('',(-0.5,0.,0.866025403784439));
#6882=DIRECTION('',(0.,-1.,0.));
#6883=DIRECTION('',(0.5,0.,-0.866025403784439));
#6884=DIRECTION('center_axis',(-0.866025403784439,0.,0.5));
#6885=DIRECTION('ref_axis',(-0.5,0.,-0.866025403784439));
#6886=DIRECTION('',(0.5,0.,0.866025403784439));
#6887=DIRECTION('',(0.,-1.,0.));
#6888=DIRECTION('',(-0.5,0.,-0.866025403784439));
#6889=DIRECTION('center_axis',(-1.60246890531964E-16,0.,1.));
#6890=DIRECTION('ref_axis',(-1.,0.,-1.60246890531964E-16));
#6891=DIRECTION('',(1.,0.,1.60246890531964E-16));
#6892=DIRECTION('',(0.,-1.,0.));
#6893=DIRECTION('',(-1.,0.,-1.60246890531964E-16));
#6894=DIRECTION('center_axis',(0.866025403784439,0.,0.5));
#6895=DIRECTION('ref_axis',(-0.5,0.,0.866025403784439));
#6896=DIRECTION('',(0.5,0.,-0.866025403784439));
#6897=DIRECTION('',(-0.5,0.,0.866025403784439));
#6898=DIRECTION('center_axis',(0.,1.,0.));
#6899=DIRECTION('ref_axis',(1.,0.,0.));
#6900=DIRECTION('center_axis',(0.,-1.,0.));
#6901=DIRECTION('ref_axis',(0.,0.,-1.));
#6902=DIRECTION('center_axis',(0.,1.,0.));
#6903=DIRECTION('ref_axis',(1.,0.,0.));
#6904=DIRECTION('center_axis',(0.,1.,0.));
#6905=DIRECTION('ref_axis',(1.,0.,0.));
#6906=DIRECTION('center_axis',(0.,1.,0.));
#6907=DIRECTION('ref_axis',(0.,0.,1.));
#6908=DIRECTION('center_axis',(0.,-1.,0.));
#6909=DIRECTION('ref_axis',(1.,0.,0.));
#6910=DIRECTION('center_axis',(0.,-1.,0.));
#6911=DIRECTION('ref_axis',(1.,0.,0.));
#6912=DIRECTION('center_axis',(0.,-1.,0.));
#6913=DIRECTION('ref_axis',(1.,0.,0.));
#6914=DIRECTION('',(0.707106781186547,0.707106781186548,8.65956056235493E-17));
#6915=DIRECTION('center_axis',(0.,-1.,0.));
#6916=DIRECTION('ref_axis',(1.,0.,0.));
#6917=DIRECTION('center_axis',(0.,-1.,0.));
#6918=DIRECTION('ref_axis',(1.,0.,0.));
#6919=DIRECTION('',(0.,1.,0.));
#6920=DIRECTION('center_axis',(0.,1.,0.));
#6921=DIRECTION('ref_axis',(1.,0.,0.));
#6922=DIRECTION('center_axis',(0.,-1.,0.));
#6923=DIRECTION('ref_axis',(1.,0.,0.));
#6924=DIRECTION('',(-0.707106781186547,0.707106781186548,-8.65956056235493E-17));
#6925=DIRECTION('center_axis',(0.,-1.,0.));
#6926=DIRECTION('ref_axis',(0.,0.,-1.));
#6927=DIRECTION('center_axis',(0.,-1.,0.));
#6928=DIRECTION('ref_axis',(1.,0.,0.));
#6929=DIRECTION('center_axis',(0.,1.,0.));
#6930=DIRECTION('ref_axis',(1.,0.,0.));
#6931=DIRECTION('center_axis',(0.,1.,0.));
#6932=DIRECTION('ref_axis',(1.,0.,0.));
#6933=DIRECTION('',(-0.447213595499958,0.894427190999916,-5.47678698264203E-17));
#6934=DIRECTION('center_axis',(0.,-1.,0.));
#6935=DIRECTION('ref_axis',(1.,0.,0.));
#6936=DIRECTION('',(0.,1.,0.));
#9356=CARTESIAN_POINT('',(0.,0.,0.));
#9357=CARTESIAN_POINT('Origin',(0.0866025403784439,-0.4,-0.15));
#9358=CARTESIAN_POINT('',(0.173205080756888,-0.4,0.));
#9359=CARTESIAN_POINT('',(0.0866025403784439,-0.4,-0.15));
#9360=CARTESIAN_POINT('',(0.173205080756888,-0.4,0.));
#9361=CARTESIAN_POINT('',(0.0866025403784439,-0.64,-0.15));
#9362=CARTESIAN_POINT('',(0.0866025403784439,-0.4,-0.15));
#9363=CARTESIAN_POINT('',(0.173205080756888,-0.64,0.));
#9364=CARTESIAN_POINT('',(0.173205080756888,-0.64,0.));
#9365=CARTESIAN_POINT('',(0.173205080756888,-0.4,0.));
#9366=CARTESIAN_POINT('Origin',(-0.0866025403784438,-0.4,-0.15));
#9367=CARTESIAN_POINT('',(-0.0866025403784438,-0.4,-0.15));
#9368=CARTESIAN_POINT('',(0.0866025403784439,-0.4,-0.15));
#9369=CARTESIAN_POINT('',(-0.0866025403784438,-0.64,-0.15));
#9370=CARTESIAN_POINT('',(-0.0866025403784438,-0.4,-0.15));
#9371=CARTESIAN_POINT('',(0.0866025403784439,-0.64,-0.15));
#9372=CARTESIAN_POINT('Origin',(-0.173205080756888,-0.4,-2.77555756156289E-17));
#9373=CARTESIAN_POINT('',(-0.173205080756888,-0.4,-2.12115047744981E-17));
#9374=CARTESIAN_POINT('',(-0.0866025403784438,-0.4,-0.15));
#9375=CARTESIAN_POINT('',(-0.173205080756888,-0.64,-2.77555756156289E-17));
#9376=CARTESIAN_POINT('',(-0.173205080756888,-0.4,-2.12115047744981E-17));
#9377=CARTESIAN_POINT('',(-0.0866025403784438,-0.64,-0.15));
#9378=CARTESIAN_POINT('Origin',(-0.0866025403784439,-0.4,0.15));
#9379=CARTESIAN_POINT('',(-0.0866025403784439,-0.4,0.15));
#9380=CARTESIAN_POINT('',(-0.173205080756888,-0.4,-2.12115047744981E-17));
#9381=CARTESIAN_POINT('',(-0.0866025403784439,-0.64,0.15));
#9382=CARTESIAN_POINT('',(-0.0866025403784439,-0.4,0.15));
#9383=CARTESIAN_POINT('',(-0.173205080756888,-0.64,-2.12115047744981E-17));
#9384=CARTESIAN_POINT('Origin',(0.0866025403784439,-0.4,0.15));
#9385=CARTESIAN_POINT('',(0.0866025403784439,-0.4,0.15));
#9386=CARTESIAN_POINT('',(-0.0866025403784439,-0.4,0.15));
#9387=CARTESIAN_POINT('',(0.0866025403784439,-0.64,0.15));
#9388=CARTESIAN_POINT('',(0.0866025403784439,-0.4,0.15));
#9389=CARTESIAN_POINT('',(-0.0866025403784439,-0.64,0.15));
#9390=CARTESIAN_POINT('Origin',(0.173205080756888,-0.4,0.));
#9391=CARTESIAN_POINT('',(0.0866025403784439,-0.4,0.15));
#9392=CARTESIAN_POINT('',(0.0866025403784439,-0.64,0.15));
#9393=CARTESIAN_POINT('Origin',(0.,-0.4,-2.77555756156289E-17));
#9394=CARTESIAN_POINT('Origin',(0.,-0.64,-2.77555756156289E-17));
#9395=CARTESIAN_POINT('Origin',(0.,-1.,0.));
#9396=CARTESIAN_POINT('',(-0.1954,-1.,2.39295984553393E-17));
#9397=CARTESIAN_POINT('Origin',(0.,-1.,0.));
#9398=CARTESIAN_POINT('Origin',(0.3,0.4,0.));
#9399=CARTESIAN_POINT('',(-0.3,0.4,-3.67394039744206E-17));
#9400=CARTESIAN_POINT('Origin',(0.,0.4,0.));
#9401=CARTESIAN_POINT('Origin',(0.,0.375,0.));
#9402=CARTESIAN_POINT('',(-0.35,0.35,-4.28626379701573E-17));
#9403=CARTESIAN_POINT('Origin',(0.,0.35,0.));
#9404=CARTESIAN_POINT('',(-0.325,0.375,-3.9801020972289E-17));
#9405=CARTESIAN_POINT('Origin',(0.,0.19,0.));
#9406=CARTESIAN_POINT('',(-0.35,0.03,-4.28626379701574E-17));
#9407=CARTESIAN_POINT('Origin',(0.,0.03,0.));
#9408=CARTESIAN_POINT('',(-0.35,0.19,-4.28626379701574E-17));
#9409=CARTESIAN_POINT('Origin',(0.,0.0149999999999999,0.));
#9410=CARTESIAN_POINT('',(-0.32,-3.29597460435593E-17,-3.91886975727153E-17));
#9411=CARTESIAN_POINT('Origin',(0.,0.,0.));
#9412=CARTESIAN_POINT('',(-0.335,0.0149999999999999,-4.10256677714363E-17));
#9413=CARTESIAN_POINT('Origin',(0.22,0.,0.));
#9414=CARTESIAN_POINT('',(-0.22,-6.93889390390723E-18,-2.69422295812418E-17));
#9415=CARTESIAN_POINT('Origin',(0.,0.,0.));
#9416=CARTESIAN_POINT('Origin',(0.,-0.02,0.));
#9417=CARTESIAN_POINT('',(-0.1954,-0.0492,2.39295984553393E-17));
#9418=CARTESIAN_POINT('Origin',(0.,-0.0492,0.));
#9419=CARTESIAN_POINT('',(-0.21,-0.02,-2.57175827820944E-17));
#9420=CARTESIAN_POINT('Origin',(0.,-0.8,0.));
#9421=CARTESIAN_POINT('',(-0.1954,-0.8,-2.39295984553393E-17));
#9769=UNCERTAINTY_MEASURE_WITH_UNIT(LENGTH_MEASURE(0.001),#9814,
'DISTANCE_ACCURACY_VALUE',
'Maximum model space distance between geometric entities at asserted c
onnectivities');
#9777=UNCERTAINTY_MEASURE_WITH_UNIT(LENGTH_MEASURE(0.001),#9814,
'DISTANCE_ACCURACY_VALUE',
'Maximum model space distance between geometric entities at asserted c
onnectivities');
#9805=(
GEOMETRIC_REPRESENTATION_CONTEXT(3)
GLOBAL_UNCERTAINTY_ASSIGNED_CONTEXT((#9769))
GLOBAL_UNIT_ASSIGNED_CONTEXT((#9814,#9816,#9817))
REPRESENTATION_CONTEXT('','3D')
);
#9813=(
GEOMETRIC_REPRESENTATION_CONTEXT(3)
GLOBAL_UNCERTAINTY_ASSIGNED_CONTEXT((#9777))
GLOBAL_UNIT_ASSIGNED_CONTEXT((#9814,#9816,#9817))
REPRESENTATION_CONTEXT('','3D')
);
#9814=(
LENGTH_UNIT()
NAMED_UNIT(*)
SI_UNIT(.CENTI.,.METRE.)
);
#9816=(
NAMED_UNIT(*)
PLANE_ANGLE_UNIT()
SI_UNIT($,.RADIAN.)
);
#9817=(
NAMED_UNIT(*)
SI_UNIT($,.STERADIAN.)
SOLID_ANGLE_UNIT()
);
#9845=SHAPE_DEFINITION_REPRESENTATION(#9885,#9962);
#9885=PRODUCT_DEFINITION_SHAPE('',$,#9998);
#9962=SHAPE_REPRESENTATION('',(#5576),#9805);
#9970=PRODUCT_DEFINITION_CONTEXT('part definition',#10077,'design');
#9998=PRODUCT_DEFINITION('M4x10 Cap Screw','M4x10 Cap Screw',#10033,#9970);
#10033=PRODUCT_DEFINITION_FORMATION('',$,#10106);
#10077=APPLICATION_CONTEXT(
'Core Data for Automotive Mechanical Design Process');
#10078=PRODUCT_CONTEXT('part definition',#10077,'mechanical');
#10106=PRODUCT('M4x10 Cap Screw','M4x10 Cap Screw','M4x10 Cap Screw',(#10078));
#10184=COLOUR_RGB('Black',0.12,0.14,0.17);
#10185=FILL_AREA_STYLE_COLOUR('',#10184);
#10186=FILL_AREA_STYLE('',(#10185));
#10187=SURFACE_STYLE_FILL_AREA(#10186);
#10188=SURFACE_SIDE_STYLE('',(#10187));
#10189=SURFACE_STYLE_USAGE(.BOTH.,#10188);
#10190=PRESENTATION_STYLE_ASSIGNMENT((#10189));
ENDSEC;
END-ISO-10303-21;
